ISO-10303-21;
HEADER;
/* Generated by software containing ST-Developer
 * from STEP Tools, Inc. (www.steptools.com) 
 */

FILE_DESCRIPTION(
/* description */ ('Cam-and-follower valve demonstrator'),
/* implementation_level */ '2;1');

FILE_NAME(
/* name */ 'Spring seat washer.step',
/* time_stamp */ '2026-10-28T03:25:17-07:00',
/* author */ (''),
/* organization */ (''),
/* preprocessor_version */ 'ST-DEVELOPER v20.2',
/* originating_system */ 'Autodesk Translation Framework v15.17.0.0',
/* authorisation */ '');

FILE_SCHEMA (('AUTOMOTIVE_DESIGN { 1 0 10303 214 3 1 1 }'));
ENDSEC;

DATA;
#10=MECHANICAL_DESIGN_GEOMETRIC_PRESENTATION_REPRESENTATION('',(#454),#12896);
#375=SHAPE_REPRESENTATION_RELATIONSHIP('SRR','None',#13095,#411);
#411=ADVANCED_BREP_SHAPE_REPRESENTATION('',(#494),#12895);
#454=STYLED_ITEM('',(#13337),#494);
#494=MANIFOLD_SOLID_BREP('Body1',#6224);
#657=FACE_BOUND('',#1992,.T.);
#658=FACE_BOUND('',#1994,.T.);
#969=CIRCLE('',#7401,0.605);
#970=CIRCLE('',#7402,0.605);
#971=CIRCLE('',#7404,1.25);
#972=CIRCLE('',#7405,1.25);
#1093=CYLINDRICAL_SURFACE('',#7400,0.605);
#1094=CYLINDRICAL_SURFACE('',#7403,1.25);
#1459=FACE_OUTER_BOUND('',#1989,.T.);
#1460=FACE_OUTER_BOUND('',#1990,.T.);
#1461=FACE_OUTER_BOUND('',#1991,.T.);
#1462=FACE_OUTER_BOUND('',#1993,.T.);
#1989=EDGE_LOOP('',(#5585,#5586,#5587,#5588));
#1990=EDGE_LOOP('',(#5589,#5590,#5591,#5592));
#1991=EDGE_LOOP('',(#5593));
#1992=EDGE_LOOP('',(#5594));
#1993=EDGE_LOOP('',(#5595));
#1994=EDGE_LOOP('',(#5596));
#2415=LINE('',#12795,#2837);
#2416=LINE('',#12801,#2838);
#2837=VECTOR('',#9394,0.605);
#2838=VECTOR('',#9401,1.25);
#3340=VERTEX_POINT('',#12792);
#3341=VERTEX_POINT('',#12794);
#3342=VERTEX_POINT('',#12798);
#3343=VERTEX_POINT('',#12800);
#4089=EDGE_CURVE('',#3340,#3340,#969,.T.);
#4090=EDGE_CURVE('',#3340,#3341,#2415,.T.);
#4091=EDGE_CURVE('',#3341,#3341,#970,.T.);
#4092=EDGE_CURVE('',#3342,#3342,#971,.T.);
#4093=EDGE_CURVE('',#3342,#3343,#2416,.T.);
#4094=EDGE_CURVE('',#3343,#3343,#972,.T.);
#5585=ORIENTED_EDGE('',*,*,#4089,.F.);
#5586=ORIENTED_EDGE('',*,*,#4090,.T.);
#5587=ORIENTED_EDGE('',*,*,#4091,.T.);
#5588=ORIENTED_EDGE('',*,*,#4090,.F.);
#5589=ORIENTED_EDGE('',*,*,#4092,.F.);
#5590=ORIENTED_EDGE('',*,*,#4093,.T.);
#5591=ORIENTED_EDGE('',*,*,#4094,.T.);
#5592=ORIENTED_EDGE('',*,*,#4093,.F.);
#5593=ORIENTED_EDGE('',*,*,#4092,.T.);
#5594=ORIENTED_EDGE('',*,*,#4089,.T.);
#5595=ORIENTED_EDGE('',*,*,#4094,.F.);
#5596=ORIENTED_EDGE('',*,*,#4091,.F.);
#5809=PLANE('',#7406);
#5810=PLANE('',#7407);
#6175=ADVANCED_FACE('',(#1459),#1093,.F.);
#6176=ADVANCED_FACE('',(#1460),#1094,.T.);
#6177=ADVANCED_FACE('',(#1461,#657),#5809,.T.);
#6178=ADVANCED_FACE('',(#1462,#658),#5810,.F.);
#6224=CLOSED_SHELL('',(#6175,#6176,#6177,#6178));
#7399=AXIS2_PLACEMENT_3D('',#12790,#9388,#9389);
#7400=AXIS2_PLACEMENT_3D('',#12791,#9390,#9391);
#7401=AXIS2_PLACEMENT_3D('',#12793,#9392,#9393);
#7402=AXIS2_PLACEMENT_3D('',#12796,#9395,#9396);
#7403=AXIS2_PLACEMENT_3D('',#12797,#9397,#9398);
#7404=AXIS2_PLACEMENT_3D('',#12799,#9399,#9400);
#7405=AXIS2_PLACEMENT_3D('',#12802,#9402,#9403);
#7406=AXIS2_PLACEMENT_3D('',#12803,#9404,#9405);
#7407=AXIS2_PLACEMENT_3D('',#12804,#9406,#9407);
#9388=DIRECTION('axis',(0.,0.,1.));
#9389=DIRECTION('refdir',(1.,0.,0.));
#9390=DIRECTION('center_axis',(0.,0.,1.));
#9391=DIRECTION('ref_axis',(1.,0.,0.));
#9392=DIRECTION('center_axis',(0.,0.,-1.));
#9393=DIRECTION('ref_axis',(1.,0.,0.));
#9394=DIRECTION('',(0.,0.,-1.));
#9395=DIRECTION('center_axis',(0.,0.,-1.));
#9396=DIRECTION('ref_axis',(1.,0.,0.));
#9397=DIRECTION('center_axis',(0.,0.,1.));
#9398=DIRECTION('ref_axis',(1.,0.,0.));
#9399=DIRECTION('center_axis',(0.,0.,1.));
#9400=DIRECTION('ref_axis',(1.,0.,0.));
#9401=DIRECTION('',(0.,0.,-1.));
#9402=DIRECTION('center_axis',(0.,0.,1.));
#9403=DIRECTION('ref_axis',(1.,0.,0.));
#9404=DIRECTION('center_axis',(0.,0.,1.));
#9405=DIRECTION('ref_axis',(1.,0.,0.));
#9406=DIRECTION('center_axis',(0.,0.,1.));
#9407=DIRECTION('ref_axis',(1.,0.,0.));
#12790=CARTESIAN_POINT('',(0.,0.,0.));
#12791=CARTESIAN_POINT('Origin',(0.,0.,7.));
#12792=CARTESIAN_POINT('',(-0.605,-7.40911313484149E-17,7.2));
#12793=CARTESIAN_POINT('Origin',(0.,0.,7.2));
#12794=CARTESIAN_POINT('',(-0.605,-7.40911313484149E-17,7.));
#12795=CARTESIAN_POINT('',(-0.605,-7.40911313484149E-17,7.));
#12796=CARTESIAN_POINT('Origin',(0.,0.,7.));
#12797=CARTESIAN_POINT('Origin',(0.,0.,7.));
#12798=CARTESIAN_POINT('',(-1.25,-1.53080849893419E-16,7.2));
#12799=CARTESIAN_POINT('Origin',(0.,0.,7.2));
#12800=CARTESIAN_POINT('',(-1.25,-1.53080849893419E-16,7.));
#12801=CARTESIAN_POINT('',(-1.25,-1.53080849893419E-16,7.));
#12802=CARTESIAN_POINT('Origin',(0.,0.,7.));
#12803=CARTESIAN_POINT('Origin',(0.,0.,7.2));
#12804=CARTESIAN_POINT('Origin',(0.,0.,7.));
#12852=UNCERTAINTY_MEASURE_WITH_UNIT(LENGTH_MEASURE(0.001),#12897,
'DISTANCE_ACCURACY_VALUE',
'Maximum model space distance between geometric entities at asserted c
onnectivities');
#12853=UNCERTAINTY_MEASURE_WITH_UNIT(LENGTH_MEASURE(0.001),#12897,
'DISTANCE_ACCURACY_VALUE',
'Maximum model space distance between geometric entities at asserted c
onnectivities');
#12895=(
GEOMETRIC_REPRESENTATION_CONTEXT(3)
GLOBAL_UNCERTAINTY_ASSIGNED_CONTEXT((#12852))
GLOBAL_UNIT_ASSIGNED_CONTEXT((#12897,#12899,#12900))
REPRESENTATION_CONTEXT('','3D')
);
#12896=(
GEOMETRIC_REPRESENTATION_CONTEXT(3)
GLOBAL_UNCERTAINTY_ASSIGNED_CONTEXT((#12853))
GLOBAL_UNIT_ASSIGNED_CONTEXT((#12897,#12899,#12900))
REPRESENTATION_CONTEXT('','3D')
);
#12897=(
LENGTH_UNIT()
NAMED_UNIT(*)
SI_UNIT(.CENTI.,.METRE.)
);
#12899=(
NAMED_UNIT(*)
PLANE_ANGLE_UNIT()
SI_UNIT($,.RADIAN.)
);
#12900=(
NAMED_UNIT(*)
SI_UNIT($,.STERADIAN.)
SOLID_ANGLE_UNIT()
);
#12942=SHAPE_DEFINITION_REPRESENTATION(#13047,#13095);
#13047=PRODUCT_DEFINITION_SHAPE('',$,#13138);
#13095=SHAPE_REPRESENTATION('',(#7399),#12895);
#13096=PRODUCT_DEFINITION_CONTEXT('part definition',#13224,'design');
#13138=PRODUCT_DEFINITION('Spring seat washer','Spring seat washer',#13180,
#13096);
#13180=PRODUCT_DEFINITION_FORMATION('',$,#13267);
#13224=APPLICATION_CONTEXT(
'Core Data for Automotive Mechanical Design Process');
#13225=PRODUCT_CONTEXT('part definition',#13224,'mechanical');
#13267=PRODUCT('Spring seat washer','Spring seat washer',
'Spring seat washer',(#13225));
#13331=COLOUR_RGB('Black',0.12,0.14,0.17);
#13332=FILL_AREA_STYLE_COLOUR('',#13331);
#13333=FILL_AREA_STYLE('',(#13332));
#13334=SURFACE_STYLE_FILL_AREA(#13333);
#13335=SURFACE_SIDE_STYLE('',(#13334));
#13336=SURFACE_STYLE_USAGE(.BOTH.,#13335);
#13337=PRESENTATION_STYLE_ASSIGNMENT((#13336));
ENDSEC;
END-ISO-10303-21;
